ISO-10303-21;
HEADER;
/* Generated by software containing ST-Developer
 * from STEP Tools, Inc. (www.steptools.com) 
 */

FILE_DESCRIPTION(
/* description */ ('Drill jig with bushing plate'),
/* implementation_level */ '2;1');

FILE_NAME(
/* name */ 'Bonded foot (3).step',
/* time_stamp */ '2026-10-27T10:51:08-07:00',
/* author */ (''),
/* organization */ (''),
/* preprocessor_version */ 'ST-DEVELOPER v20.2',
/* originating_system */ 'Autodesk Translation Framework v15.17.0.0',
/* authorisation */ '');

FILE_SCHEMA (('AUTOMOTIVE_DESIGN { 1 0 10303 214 3 1 1 }'));
ENDSEC;

DATA;
#10=MECHANICAL_DESIGN_GEOMETRIC_PRESENTATION_REPRESENTATION('',(#227),#6638);
#179=SHAPE_REPRESENTATION_RELATIONSHIP('SRR','None',#6743,#203);
#203=ADVANCED_BREP_SHAPE_REPRESENTATION('',(#251),#6616);
#227=STYLED_ITEM('',(#6957),#251);
#251=MANIFOLD_SOLID_BREP('Body1',#3594);
#382=PLANE('',#3954);
#383=PLANE('',#3955);
#530=FACE_OUTER_BOUND('',#772,.T.);
#531=FACE_OUTER_BOUND('',#773,.T.);
#532=FACE_OUTER_BOUND('',#774,.T.);
#772=EDGE_LOOP('',(#2563,#2564,#2565,#2566));
#773=EDGE_LOOP('',(#2567));
#774=EDGE_LOOP('',(#2568));
#1059=LINE('',#5631,#1320);
#1320=VECTOR('',#4502,0.800000000000001);
#1586=CIRCLE('',#3952,0.800000000000001);
#1587=CIRCLE('',#3953,0.800000000000001);
#1762=VERTEX_POINT('',#5628);
#1763=VERTEX_POINT('',#5630);
#2069=EDGE_CURVE('',#1762,#1762,#1586,.T.);
#2070=EDGE_CURVE('',#1762,#1763,#1059,.T.);
#2071=EDGE_CURVE('',#1763,#1763,#1587,.T.);
#2563=ORIENTED_EDGE('',*,*,#2069,.F.);
#2564=ORIENTED_EDGE('',*,*,#2070,.T.);
#2565=ORIENTED_EDGE('',*,*,#2071,.T.);
#2566=ORIENTED_EDGE('',*,*,#2070,.F.);
#2567=ORIENTED_EDGE('',*,*,#2069,.T.);
#2568=ORIENTED_EDGE('',*,*,#2071,.F.);
#3316=CYLINDRICAL_SURFACE('',#3951,0.800000000000001);
#3405=ADVANCED_FACE('',(#530),#3316,.T.);
#3406=ADVANCED_FACE('',(#531),#382,.T.);
#3407=ADVANCED_FACE('',(#532),#383,.F.);
#3594=CLOSED_SHELL('',(#3405,#3406,#3407));
#3950=AXIS2_PLACEMENT_3D('',#5626,#4496,#4497);
#3951=AXIS2_PLACEMENT_3D('',#5627,#4498,#4499);
#3952=AXIS2_PLACEMENT_3D('',#5629,#4500,#4501);
#3953=AXIS2_PLACEMENT_3D('',#5632,#4503,#4504);
#3954=AXIS2_PLACEMENT_3D('',#5633,#4505,#4506);
#3955=AXIS2_PLACEMENT_3D('',#5634,#4507,#4508);
#4496=DIRECTION('axis',(0.,0.,1.));
#4497=DIRECTION('refdir',(1.,0.,0.));
#4498=DIRECTION('center_axis',(0.,0.,1.));
#4499=DIRECTION('ref_axis',(1.,0.,0.));
#4500=DIRECTION('center_axis',(0.,0.,1.));
#4501=DIRECTION('ref_axis',(1.,0.,0.));
#4502=DIRECTION('',(0.,0.,-1.));
#4503=DIRECTION('center_axis',(0.,0.,1.));
#4504=DIRECTION('ref_axis',(1.,0.,0.));
#4505=DIRECTION('center_axis',(0.,0.,1.));
#4506=DIRECTION('ref_axis',(1.,0.,0.));
#4507=DIRECTION('center_axis',(0.,0.,1.));
#4508=DIRECTION('ref_axis',(1.,0.,0.));
#5626=CARTESIAN_POINT('',(0.,0.,0.));
#5627=CARTESIAN_POINT('Origin',(11.,7.,-0.5));
#5628=CARTESIAN_POINT('',(10.2,7.,0.));
#5629=CARTESIAN_POINT('Origin',(11.,7.,0.));
#5630=CARTESIAN_POINT('',(10.2,7.,-0.5));
#5631=CARTESIAN_POINT('',(10.2,7.,-0.5));
#5632=CARTESIAN_POINT('Origin',(11.,7.,-0.5));
#5633=CARTESIAN_POINT('Origin',(11.,7.,0.));
#5634=CARTESIAN_POINT('Origin',(11.,7.,-0.5));
#6587=UNCERTAINTY_MEASURE_WITH_UNIT(LENGTH_MEASURE(0.001),#6639,
'DISTANCE_ACCURACY_VALUE',
'Maximum model space distance between geometric entities at asserted c
onnectivities');
#6609=UNCERTAINTY_MEASURE_WITH_UNIT(LENGTH_MEASURE(0.001),#6639,
'DISTANCE_ACCURACY_VALUE',
'Maximum model space distance between geometric entities at asserted c
onnectivities');
#6616=(
GEOMETRIC_REPRESENTATION_CONTEXT(3)
GLOBAL_UNCERTAINTY_ASSIGNED_CONTEXT((#6587))
GLOBAL_UNIT_ASSIGNED_CONTEXT((#6639,#6641,#6642))
REPRESENTATION_CONTEXT('','3D')
);
#6638=(
GEOMETRIC_REPRESENTATION_CONTEXT(3)
GLOBAL_UNCERTAINTY_ASSIGNED_CONTEXT((#6609))
GLOBAL_UNIT_ASSIGNED_CONTEXT((#6639,#6641,#6642))
REPRESENTATION_CONTEXT('','3D')
);
#6639=(
LENGTH_UNIT()
NAMED_UNIT(*)
SI_UNIT(.CENTI.,.METRE.)
);
#6641=(
NAMED_UNIT(*)
PLANE_ANGLE_UNIT()
SI_UNIT($,.RADIAN.)
);
#6642=(
NAMED_UNIT(*)
SI_UNIT($,.STERADIAN.)
SOLID_ANGLE_UNIT()
);
#6649=SHAPE_DEFINITION_REPRESENTATION(#6677,#6743);
#6677=PRODUCT_DEFINITION_SHAPE('',$,#6772);
#6743=SHAPE_REPRESENTATION('',(#3950),#6616);
#6765=PRODUCT_DEFINITION_CONTEXT('part definition',#6851,'design');
#6772=PRODUCT_DEFINITION('Bonded foot (3)','Bonded foot (3)',#6800,#6765);
#6800=PRODUCT_DEFINITION_FORMATION('',$,#6859);
#6851=APPLICATION_CONTEXT(
'Core Data for Automotive Mechanical Design Process');
#6852=PRODUCT_CONTEXT('part definition',#6851,'mechanical');
#6859=PRODUCT('Bonded foot (3)','Bonded foot (3)','Bonded foot (3)',(#6852));
#6951=COLOUR_RGB('Off White',0.89,0.88,0.83);
#6952=FILL_AREA_STYLE_COLOUR('',#6951);
#6953=FILL_AREA_STYLE('',(#6952));
#6954=SURFACE_STYLE_FILL_AREA(#6953);
#6955=SURFACE_SIDE_STYLE('',(#6954));
#6956=SURFACE_STYLE_USAGE(.BOTH.,#6955);
#6957=PRESENTATION_STYLE_ASSIGNMENT((#6956));
ENDSEC;
END-ISO-10303-21;
